ISO-10303-21;
HEADER;
FILE_DESCRIPTION (('STEP AP214'),
    '1' );
FILE_NAME ('angular contact ball bearing_68_iso_ISO 15 ABB - 1740 - 38,SI,NC,38_68.step',
    '2026-10-31T03:46:07',
    ( '' ),
    ( '' ),
    'SwSTEP 2.0',
    'SolidWorks 2026',
    '' );
FILE_SCHEMA (( 'AUTOMOTIVE_DESIGN' ));
ENDSEC;

DATA;
#71=DIRECTION ( 'NONE',  ( 1.000000000000000000, 0.000000000000000000, 0.000000000000000000 ) ) ;
#73=ORIENTED_EDGE ( 'NONE', *, *, #3413, .T. ) ;
#103=DIRECTION ( 'NONE',  ( 1.000000000000000000, 0.000000000000000000, 0.000000000000000000 ) ) ;
#137=ORIENTED_EDGE ( 'NONE', *, *, #23350, .T. ) ;
#154=ORIENTED_EDGE ( 'NONE', *, *, #8010, .T. ) ;
#220=CARTESIAN_POINT ( 'NONE',  ( 2.999999999999995559, 2.574819895207310198E-15, 21.02499999999999858 ) ) ;
#243=DIRECTION ( 'NONE',  ( 1.000000000000000000, 0.000000000000000000, 0.000000000000000000 ) ) ;
#318=DIRECTION ( 'NONE',  ( 0.000000000000000000, 0.000000000000000000, -1.000000000000000000 ) ) ;
#338=ORIENTED_EDGE ( 'NONE', *, *, #6400, .F. ) ;
#414=( LENGTH_UNIT ( ) NAMED_UNIT ( * ) SI_UNIT ( .MILLI., .METRE. ) );
#441=FACE_OUTER_BOUND ( 'NONE', #10647, .T. ) ;
#449=LINE ( 'NONE', #9746, #13276 ) ;
#479=CARTESIAN_POINT ( 'NONE',  ( -3.000000000000002665, 0.000000000000000000, 0.000000000000000000 ) ) ;
#560=DIRECTION ( 'NONE',  ( 0.000000000000000000, 0.000000000000000000, -1.000000000000000000 ) ) ;
#607=EDGE_LOOP ( 'NONE', ( #10309, #6609 ) ) ;
#650=EDGE_CURVE ( 'NONE', #19885, #23227, #1024, .T. ) ;
#664=CARTESIAN_POINT ( 'NONE',  ( 3.000000000000002665, 0.000000000000000000, 0.000000000000000000 ) ) ;
#671=CARTESIAN_POINT ( 'NONE',  ( 2.700000000000001066, 3.061616997868383043E-15, 25.00000000000000000 ) ) ;
#685=CARTESIAN_POINT ( 'NONE',  ( 0.000000000000000000, 0.000000000000000000, 0.000000000000000000 ) ) ;
#687=DIRECTION ( 'NONE',  ( -1.000000000000000000, -0.000000000000000000, -0.000000000000000000 ) ) ;
#720=DIRECTION ( 'NONE',  ( 1.000000000000000000, 0.000000000000000000, 0.000000000000000000 ) ) ;
#723=CIRCLE ( 'NONE', #22695, 0.3000000000000016542 ) ;
#725=AXIS2_PLACEMENT_3D ( 'NONE', #17069, #2691, #22955 ) ;
#727=ORIENTED_EDGE ( 'NONE', *, *, #5522, .F. ) ;
#730=CIRCLE ( 'NONE', #10814, 21.02499999999999858 ) ;
#738=AXIS2_PLACEMENT_3D ( 'NONE', #10187, #23204, #21160 ) ;
#744=DIRECTION ( 'NONE',  ( 1.000000000000000000, 0.000000000000000000, 0.000000000000000000 ) ) ;
#763=AXIS2_PLACEMENT_3D ( 'NONE', #1583, #22208, #7132 ) ;
#809=CARTESIAN_POINT ( 'NONE',  ( -20.63749999999999574, 0.000000000000000000, -23.97500000000000497 ) ) ;
#842=CARTESIAN_POINT ( 'NONE',  ( -20.63749999999999574, 3.061616997868383043E-15, 25.00000000000000000 ) ) ;
#877=DIRECTION ( 'NONE',  ( 0.000000000000000000, 0.000000000000000000, -1.000000000000000000 ) ) ;
#879=FACE_OUTER_BOUND ( 'NONE', #17446, .T. ) ;
#919=ORIENTED_EDGE ( 'NONE', *, *, #5943, .T. ) ;
#932=DIRECTION ( 'NONE',  ( 0.000000000000000000, 0.000000000000000000, -1.000000000000000000 ) ) ;
#938=ORIENTED_EDGE ( 'NONE', *, *, #5830, .F. ) ;
#945=ORIENTED_EDGE ( 'NONE', *, *, #15780, .T. ) ;
#956=ORIENTED_EDGE ( 'NONE', *, *, #20313, .F. ) ;
#1002=ORIENTED_EDGE ( 'NONE', *, *, #5522, .T. ) ;
#1024=LINE ( 'NONE', #809, #15629 ) ;
#1036=AXIS2_PLACEMENT_3D ( 'NONE', #479, #16888, #5898 ) ;
#1051=ORIENTED_EDGE ( 'NONE', *, *, #650, .F. ) ;
#1082=CIRCLE ( 'NONE', #18429, 23.50000000000000000 ) ;
#1096=DIRECTION ( 'NONE',  ( 1.000000000000000000, 0.000000000000000000, 0.000000000000000000 ) ) ;
#1151=CARTESIAN_POINT ( 'NONE',  ( -20.63749999999999574, 2.936090700955779752E-15, 23.97500000000000497 ) ) ;
#1160=PRODUCT_DEFINITION_FORMATION_WITH_SPECIFIED_SOURCE ( 'ANY', '', #23269, .NOT_KNOWN. ) ;
#1246=EDGE_CURVE ( 'NONE', #8826, #18148, #21051, .T. ) ;
#1328=DIRECTION ( 'NONE',  ( 0.000000000000000000, 0.000000000000000000, -1.000000000000000000 ) ) ;
#1345=TOROIDAL_SURFACE ( 'NONE', #8046, 22.50000000000000000, 1.500000000000000444 ) ;
#1371=DIRECTION ( 'NONE',  ( 0.000000000000000000, 0.000000000000000000, -1.000000000000000000 ) ) ;
#1377=CARTESIAN_POINT ( 'NONE',  ( 2.700000000000001510, 3.024877593893962577E-15, 24.69999999999999929 ) ) ;
#1407=DIRECTION ( 'NONE',  ( 0.000000000000000000, 0.000000000000000000, -1.000000000000000000 ) ) ;
#1418=DIRECTION ( 'NONE',  ( 0.000000000000000000, 0.000000000000000000, -1.000000000000000000 ) ) ;
#1474=CIRCLE ( 'NONE', #18053, 0.3000000000000051514 ) ;
#1515=AXIS2_PLACEMENT_3D ( 'NONE', #23513, #21696, #12679 ) ;
#1517=DIRECTION ( 'NONE',  ( 0.000000000000000000, 0.000000000000000000, -1.000000000000000000 ) ) ;
#1583=CARTESIAN_POINT ( 'NONE',  ( 1.118033988749894458, 0.000000000000000000, 0.000000000000000000 ) ) ;
#1606=ORIENTED_EDGE ( 'NONE', *, *, #3413, .F. ) ;
#1620=DIRECTION ( 'NONE',  ( 1.000000000000000000, 0.000000000000000000, 0.000000000000000000 ) ) ;
#1626=CARTESIAN_POINT ( 'NONE',  ( 3.000000000000002665, 0.000000000000000000, 0.000000000000000000 ) ) ;
#1645=CARTESIAN_POINT ( 'NONE',  ( -20.63749999999999929, 0.000000000000000000, -21.02499999999999503 ) ) ;
#1666=CARTESIAN_POINT ( 'NONE',  ( -3.000000000000002665, 0.000000000000000000, 0.000000000000000000 ) ) ;
#1689=CARTESIAN_POINT ( 'NONE',  ( 2.700000000000001066, 0.000000000000000000, -25.00000000000000000 ) ) ;
#1697=SURFACE_STYLE_USAGE ( .BOTH. , #14528 ) ;
#1710=DIRECTION ( 'NONE',  ( 1.000000000000000000, 0.000000000000000000, 0.000000000000000000 ) ) ;
#1728=ADVANCED_FACE ( 'NONE', ( #13407 ), #1345, .T. ) ;
#1750=DIRECTION ( 'NONE',  ( 1.000000000000000000, 0.000000000000000000, 0.000000000000000000 ) ) ;
#1761=AXIS2_PLACEMENT_3D ( 'NONE', #19347, #17542, #21521 ) ;
#1770=ADVANCED_FACE ( 'NONE', ( #7937 ), #18780, .T. ) ;
#1805=CIRCLE ( 'NONE', #6059, 21.50000000000000000 ) ;
#1866=AXIS2_PLACEMENT_3D ( 'NONE', #21039, #4499, #11907 ) ;
#1916=ADVANCED_FACE ( 'NONE', ( #15095 ), #12665, .F. ) ;
#1923=DIRECTION ( 'NONE',  ( 0.000000000000000000, 1.224646799147357891E-16, 1.000000000000000000 ) ) ;
#1927=CIRCLE ( 'NONE', #13566, 23.50000000000000000 ) ;
#1962=LINE ( 'NONE', #5240, #17573 ) ;
#1975=EDGE_CURVE ( 'NONE', #3512, #8656, #1082, .T. ) ;
#2018=DIRECTION ( 'NONE',  ( 1.000000000000000000, 0.000000000000000000, 0.000000000000000000 ) ) ;
#2026=AXIS2_PLACEMENT_3D ( 'NONE', #8177, #8284, #19258 ) ;
#2035=FACE_OUTER_BOUND ( 'NONE', #3165, .T. ) ;
#2042=TOROIDAL_SURFACE ( 'NONE', #23274, 20.30000000000000071, 0.3000000000000059841 ) ;
#2052=EDGE_LOOP ( 'NONE', ( #2396, #7471, #17213, #12512 ) ) ;
#2062=DIRECTION ( 'NONE',  ( 0.000000000000000000, 0.000000000000000000, -1.000000000000000000 ) ) ;
#2073=ADVANCED_BREP_SHAPE_REPRESENTATION ( '', ( #20279, #11210 ), #9278 ) ;
#2105=CARTESIAN_POINT ( 'NONE',  ( -3.000000000000002665, 0.000000000000000000, -23.97500000000000142 ) ) ;
#2110=DIRECTION ( 'NONE',  ( 0.000000000000000000, 0.000000000000000000, -1.000000000000000000 ) ) ;
#2169=SHAPE_REPRESENTATION_RELATIONSHIP ( 'NONE' , 'NONE' ,  #14711, #2073 ) ;
#2265=CARTESIAN_POINT ( 'NONE',  ( 3.000000000000001776, 24.69999999999999929, 0.000000000000000000 ) ) ;
#2362=FACE_OUTER_BOUND ( 'NONE', #23526, .T. ) ;
#2383=UNCERTAINTY_MEASURE_WITH_UNIT (LENGTH_MEASURE( 1.000000000000000082E-05 ), #20647, 'distance_accuracy_value', 'NONE');
#2396=ORIENTED_EDGE ( 'NONE', *, *, #8047, .F. ) ;
#2438=CARTESIAN_POINT ( 'NONE',  ( -3.000000000000002665, 0.000000000000000000, 0.000000000000000000 ) ) ;
#2499=DIRECTION ( 'NONE',  ( 0.000000000000000000, 0.000000000000000000, 1.000000000000000000 ) ) ;
#2573=AXIS2_PLACEMENT_3D ( 'NONE', #18121, #3715, #20260 ) ;
#2595=ORIENTED_EDGE ( 'NONE', *, *, #1246, .T. ) ;
#2603=AXIS2_PLACEMENT_3D ( 'NONE', #15932, #23273, #4930 ) ;
#2616=DIRECTION ( 'NONE',  ( 1.000000000000000000, 0.000000000000000000, 0.000000000000000000 ) ) ;
#2685=UNCERTAINTY_MEASURE_WITH_UNIT (LENGTH_MEASURE( 1.000000000000000082E-05 ), #414, 'distance_accuracy_value', 'NONE');
#2691=DIRECTION ( 'NONE',  ( -1.000000000000000000, -0.000000000000000000, -0.000000000000000000 ) ) ;
#2704=FACE_OUTER_BOUND ( 'NONE', #19121, .T. ) ;
#2730=EDGE_CURVE ( 'NONE', #5940, #15926, #4241, .T. ) ;
#2750=APPLICATION_CONTEXT ( 'automotive_design' ) ;
#2804=EDGE_CURVE ( 'NONE', #2929, #19885, #4112, .T. ) ;
#2827=DIRECTION ( 'NONE',  ( 0.000000000000000000, 1.224646799147346305E-16, 1.000000000000000000 ) ) ;
#2858=CARTESIAN_POINT ( 'NONE',  ( -1.118033988749894458, 0.000000000000000000, 0.000000000000000000 ) ) ;
#2889=FACE_BOUND ( 'NONE', #11034, .T. ) ;
#2891=EDGE_CURVE ( 'NONE', #13630, #11363, #5728, .T. ) ;
#2929=VERTEX_POINT ( 'NONE', #19032 ) ;
#2937=CARTESIAN_POINT ( 'NONE',  ( -20.63749999999999929, 0.000000000000000000, 0.000000000000000000 ) ) ;
#3003=CIRCLE ( 'NONE', #14595, 1.500000000000001332 ) ;
#3032=ORIENTED_EDGE ( 'NONE', *, *, #21249, .F. ) ;
#3099=EDGE_LOOP ( 'NONE', ( #14042, #21270 ) ) ;
#3165=EDGE_LOOP ( 'NONE', ( #12116, #5371, #23614, #16895 ) ) ;
#3186=CIRCLE ( 'NONE', #2026, 25.00000000000000000 ) ;
#3211=LINE ( 'NONE', #1645, #17103 ) ;
#3279=CARTESIAN_POINT ( 'NONE',  ( 2.699999999999995737, 0.000000000000000000, -20.30000000000000071 ) ) ;
#3332=DIRECTION ( 'NONE',  ( 1.000000000000000000, 0.000000000000000000, 0.000000000000000000 ) ) ;
#3336=DIRECTION ( 'NONE',  ( 0.000000000000000000, -1.000000000000000000, 0.000000000000000000 ) ) ;
#3389=( NAMED_UNIT ( * ) SI_UNIT ( $, .STERADIAN. ) SOLID_ANGLE_UNIT ( ) );
#3413=EDGE_CURVE ( 'NONE', #4308, #21081, #13121, .T. ) ;
#3420=PRODUCT_DEFINITION_SHAPE ( 'NONE', 'NONE',  #9630 ) ;
#3437=STYLED_ITEM('',(#23920),#20279);
#3472=CARTESIAN_POINT ( 'NONE',  ( 3.000000000000002665, 3.043247295881173007E-15, 24.69999999999999929 ) ) ;
#3507=EDGE_CURVE ( 'NONE', #13434, #18427, #730, .T. ) ;
#3512=VERTEX_POINT ( 'NONE', #14002 ) ;
#3526=DIRECTION ( 'NONE',  ( 0.000000000000000000, 0.000000000000000000, -1.000000000000000000 ) ) ;
#3658=AXIS2_PLACEMENT_3D ( 'NONE', #18692, #243, #5808 ) ;
#3715=DIRECTION ( 'NONE',  ( 0.000000000000000000, 1.000000000000000000, -1.224646799147353207E-16 ) ) ;
#3761=DIRECTION ( 'NONE',  ( 1.000000000000000000, 0.000000000000000000, 0.000000000000000000 ) ) ;
#3769=DIRECTION ( 'NONE',  ( 1.000000000000000000, 0.000000000000000000, 0.000000000000000000 ) ) ;
#3775=CARTESIAN_POINT ( 'NONE',  ( 3.000000000000002665, 0.000000000000000000, 0.000000000000000000 ) ) ;
#3790=STYLED_ITEM ( 'NONE', ( #9208 ), #2073 ) ;
#3801=DIRECTION ( 'NONE',  ( 0.000000000000000000, -1.000000000000000000, 0.000000000000000000 ) ) ;
#3806=DIRECTION ( 'NONE',  ( 0.000000000000000000, 0.000000000000000000, -1.000000000000000000 ) ) ;
#3818=TOROIDAL_SURFACE ( 'NONE', #6540, 24.69999999999999929, 0.3000000000000007661 ) ;
#3858=MECHANICAL_DESIGN_GEOMETRIC_PRESENTATION_REPRESENTATION('',(#3790),#11959);
#3875=( LENGTH_UNIT ( ) NAMED_UNIT ( * ) SI_UNIT ( .MILLI., .METRE. ) );
#3890=DIRECTION ( 'NONE',  ( 0.000000000000000000, -1.000000000000000000, 0.000000000000000000 ) ) ;
#3896=CARTESIAN_POINT ( 'NONE',  ( 0.2727178028658734932, 2.726369936601794865E-15, -21.02499999999999503 ) ) ;
#3904=DIRECTION ( 'NONE',  ( 0.000000000000000000, 0.000000000000000000, -1.000000000000000000 ) ) ;
#3922=CARTESIAN_POINT ( 'NONE',  ( -20.63749999999999574, 0.000000000000000000, 0.000000000000000000 ) ) ;
#3938=EDGE_CURVE ( 'NONE', #17297, #23365, #5770, .T. ) ;
#3992=EDGE_CURVE ( 'NONE', #22350, #13630, #23092, .T. ) ;
#3996=ORIENTED_EDGE ( 'NONE', *, *, #6944, .F. ) ;
#4024=DIRECTION ( 'NONE',  ( 0.000000000000000000, 0.000000000000000000, -1.000000000000000000 ) ) ;
#4090=CARTESIAN_POINT ( 'NONE',  ( -20.63749999999999574, 0.000000000000000000, 0.000000000000000000 ) ) ;
#4112=CIRCLE ( 'NONE', #17621, 23.97500000000000142 ) ;
#4145=CIRCLE ( 'NONE', #9185, 19.99999999999999645 ) ;
#4162=DIRECTION ( 'NONE',  ( 1.000000000000000000, 0.000000000000000000, 0.000000000000000000 ) ) ;
#4183=DIRECTION ( 'NONE',  ( -1.000000000000000000, -0.000000000000000000, -0.000000000000000000 ) ) ;
#4230=DIRECTION ( 'NONE',  ( 1.000000000000000000, 0.000000000000000000, 0.000000000000000000 ) ) ;
#4241=CIRCLE ( 'NONE', #17753, 24.69999999999999929 ) ;
#4259=ADVANCED_FACE ( 'NONE', ( #5714 ), #3818, .T. ) ;
#4298=CARTESIAN_POINT ( 'NONE',  ( 0.000000000000000000, 0.000000000000000000, 0.000000000000000000 ) ) ;
#4308=VERTEX_POINT ( 'NONE', #1689 ) ;
#4342=EDGE_LOOP ( 'NONE', ( #14493, #19486, #1002, #23440 ) ) ;
#4402=ORIENTED_EDGE ( 'NONE', *, *, #6799, .T. ) ;
#4465=ADVANCED_FACE ( 'NONE', ( #2035 ), #7139, .T. ) ;
#4481=FACE_OUTER_BOUND ( 'NONE', #15999, .T. ) ;
#4499=DIRECTION ( 'NONE',  ( -1.000000000000000000, -0.000000000000000000, -0.000000000000000000 ) ) ;
#4574=CIRCLE ( 'NONE', #725, 23.97500000000000497 ) ;
#4625=FACE_OUTER_BOUND ( 'NONE', #6996, .T. ) ;
#4652=EDGE_LOOP ( 'NONE', ( #11629, #14445, #22052, #17757 ) ) ;
#4670=ORIENTED_EDGE ( 'NONE', *, *, #4721, .F. ) ;
#4717=ORIENTED_EDGE ( 'NONE', *, *, #3992, .T. ) ;
#4721=EDGE_CURVE ( 'NONE', #21286, #17297, #14272, .T. ) ;
#4920=CARTESIAN_POINT ( 'NONE',  ( -3.000000000000002665, 0.000000000000000000, -24.69999999999999929 ) ) ;
#4930=DIRECTION ( 'NONE',  ( -0.000000000000000000, 0.000000000000000000, 1.000000000000000000 ) ) ;
#4958=TOROIDAL_SURFACE ( 'NONE', #5723, 20.30000000000000071, 0.3000000000000059841 ) ;
#4968=COLOUR_RGB ( '',1.000000000000000000, 0.9490196078431372140, 0.9098039215686274384 ) ;
#4981=DIRECTION ( 'NONE',  ( 1.000000000000000000, 0.000000000000000000, 0.000000000000000000 ) ) ;
#4986=AXIS2_PLACEMENT_3D ( 'NONE', #13964, #4981, #12044 ) ;
#5020=DIRECTION ( 'NONE',  ( 0.000000000000000000, 0.000000000000000000, -1.000000000000000000 ) ) ;
#5040=ADVANCED_FACE ( 'NONE', ( #5121 ), #6389, .T. ) ;
#5070=ORIENTED_EDGE ( 'NONE', *, *, #1975, .T. ) ;
#5121=FACE_OUTER_BOUND ( 'NONE', #5447, .T. ) ;
#5155=EDGE_CURVE ( 'NONE', #22350, #18427, #1962, .T. ) ;
#5187=CIRCLE ( 'NONE', #23681, 21.02499999999999858 ) ;
#5240=CARTESIAN_POINT ( 'NONE',  ( -20.63749999999999929, 2.574819895207309803E-15, 21.02499999999999503 ) ) ;
#5253=ORIENTED_EDGE ( 'NONE', *, *, #7872, .T. ) ;
#5262=VERTEX_POINT ( 'NONE', #16944 ) ;
#5268=EDGE_LOOP ( 'NONE', ( #6337, #19567, #21082, #1051 ) ) ;
#5279=CIRCLE ( 'NONE', #18747, 19.99999999999998934 ) ;
#5300=VERTEX_POINT ( 'NONE', #6304 ) ;
#5343=DIRECTION ( 'NONE',  ( 0.000000000000000000, 0.000000000000000000, -1.000000000000000000 ) ) ;
#5371=ORIENTED_EDGE ( 'NONE', *, *, #12478, .T. ) ;
#5419=CARTESIAN_POINT ( 'NONE',  ( -20.63749999999999574, 2.877919977996280320E-15, 23.50000000000000000 ) ) ;
#5441=DIRECTION ( 'NONE',  ( 1.000000000000000000, 0.000000000000000000, 0.000000000000000000 ) ) ;
#5447=EDGE_LOOP ( 'NONE', ( #18996, #8728, #7045, #14544 ) ) ;
#5460=CYLINDRICAL_SURFACE ( 'NONE', #21600, 23.97500000000000497 ) ;
#5522=EDGE_CURVE ( 'NONE', #11363, #13630, #21979, .T. ) ;
#5525=CIRCLE ( 'NONE', #22852, 20.30000000000000071 ) ;
#5637=ADVANCED_FACE ( 'NONE', ( #7974 ), #9687, .T. ) ;
#5645=CARTESIAN_POINT ( 'NONE',  ( 2.699999999999997513, 0.000000000000000000, 0.000000000000000000 ) ) ;
#5679=CIRCLE ( 'NONE', #22248, 0.3000000000000016542 ) ;
#5689=CIRCLE ( 'NONE', #20733, 0.3000000000000051514 ) ;
#5700=ORIENTED_EDGE ( 'NONE', *, *, #17469, .T. ) ;
#5702=DIRECTION ( 'NONE',  ( 0.000000000000000000, 0.000000000000000000, -1.000000000000000000 ) ) ;
#5714=FACE_OUTER_BOUND ( 'NONE', #7928, .T. ) ;
#5723=AXIS2_PLACEMENT_3D ( 'NONE', #6012, #2018, #7461 ) ;
#5728=CIRCLE ( 'NONE', #6507, 23.50000000000000000 ) ;
#5752=DIRECTION ( 'NONE',  ( 0.000000000000000000, 0.000000000000000000, -1.000000000000000000 ) ) ;
#5770=CIRCLE ( 'NONE', #21574, 21.50000000000000000 ) ;
#5774=CARTESIAN_POINT ( 'NONE',  ( -20.63749999999999574, 0.000000000000000000, 0.000000000000000000 ) ) ;
#5781=CARTESIAN_POINT ( 'NONE',  ( 1.118033988749894458, 0.000000000000000000, 0.000000000000000000 ) ) ;
#5786=CARTESIAN_POINT ( 'NONE',  ( 3.000000000000002665, 0.000000000000000000, -24.69999999999999929 ) ) ;
#5808=DIRECTION ( 'NONE',  ( 0.000000000000000000, 0.000000000000000000, -1.000000000000000000 ) ) ;
#5830=EDGE_CURVE ( 'NONE', #9561, #21081, #10405, .T. ) ;
#5898=DIRECTION ( 'NONE',  ( 0.000000000000000000, 0.000000000000000000, -1.000000000000000000 ) ) ;
#5925=DIRECTION ( 'NONE',  ( -1.000000000000000000, -0.000000000000000000, -0.000000000000000000 ) ) ;
#5939=CARTESIAN_POINT ( 'NONE',  ( -20.63749999999999574, 0.000000000000000000, 0.000000000000000000 ) ) ;
#5940=VERTEX_POINT ( 'NONE', #5786 ) ;
#5943=EDGE_CURVE ( 'NONE', #14308, #7318, #7712, .T. ) ;
#5977=DIRECTION ( 'NONE',  ( 1.000000000000000000, 0.000000000000000000, 0.000000000000000000 ) ) ;
#6012=CARTESIAN_POINT ( 'NONE',  ( -2.699999999999995737, 0.000000000000000000, 0.000000000000000000 ) ) ;
#6059=AXIS2_PLACEMENT_3D ( 'NONE', #2858, #12105, #932 ) ;
#6077=DIRECTION ( 'NONE',  ( 0.000000000000000000, 0.000000000000000000, -1.000000000000000000 ) ) ;
#6098=DIRECTION ( 'NONE',  ( 1.000000000000000000, 0.000000000000000000, 0.000000000000000000 ) ) ;
#6102=LINE ( 'NONE', #9982, #6481 ) ;
#6107=AXIS2_PLACEMENT_3D ( 'NONE', #20104, #71, #18182 ) ;
#6110=DIRECTION ( 'NONE',  ( 1.000000000000000000, 0.000000000000000000, 0.000000000000000000 ) ) ;
#6125=CIRCLE ( 'NONE', #8068, 20.30000000000000071 ) ;
#6130=DIRECTION ( 'NONE',  ( 1.000000000000000000, 0.000000000000000000, 0.000000000000000000 ) ) ;
#6229=DIRECTION ( 'NONE',  ( 0.000000000000000000, 0.000000000000000000, -1.000000000000000000 ) ) ;
#6293=ADVANCED_FACE ( 'NONE', ( #8921 ), #21570, .T. ) ;
#6297=DIRECTION ( 'NONE',  ( 0.000000000000000000, 0.000000000000000000, -1.000000000000000000 ) ) ;
#6304=CARTESIAN_POINT ( 'NONE',  ( 3.000000000000002220, 2.486033002269127373E-15, 20.30000000000000071 ) ) ;
#6337=ORIENTED_EDGE ( 'NONE', *, *, #2804, .F. ) ;
#6389=TOROIDAL_SURFACE ( 'NONE', #12611, 24.69999999999999929, 0.3000000000000007661 ) ;
#6400=EDGE_CURVE ( 'NONE', #21286, #22490, #9240, .T. ) ;
#6475=DIRECTION ( 'NONE',  ( 0.000000000000000000, 0.000000000000000000, 1.000000000000000000 ) ) ;
#6480=LINE ( 'NONE', #19387, #10603 ) ;
#6481=VECTOR ( 'NONE', #15542, 1000.000000000000000 ) ;
#6507=AXIS2_PLACEMENT_3D ( 'NONE', #5781, #6130, #2499 ) ;
#6513=ORIENTED_EDGE ( 'NONE', *, *, #22859, .F. ) ;
#6540=AXIS2_PLACEMENT_3D ( 'NONE', #20554, #22125, #18384 ) ;
#6604=DIRECTION ( 'NONE',  ( 1.000000000000000000, 0.000000000000000000, 0.000000000000000000 ) ) ;
#6607=CARTESIAN_POINT ( 'NONE',  ( 2.700000000000001066, 0.000000000000000000, 0.000000000000000000 ) ) ;
#6609=ORIENTED_EDGE ( 'NONE', *, *, #12306, .T. ) ;
#6735=EDGE_LOOP ( 'NONE', ( #938, #154, #21324, #18695 ) ) ;
#6743=DIRECTION ( 'NONE',  ( 1.000000000000000000, 0.000000000000000000, 0.000000000000000000 ) ) ;
#6784=( NAMED_UNIT ( * ) SI_UNIT ( $, .STERADIAN. ) SOLID_ANGLE_UNIT ( ) );
#6799=EDGE_CURVE ( 'NONE', #21081, #4308, #22825, .T. ) ;
#6813=AXIS2_PLACEMENT_3D ( 'NONE', #18497, #15369, #9454 ) ;
#6846=CARTESIAN_POINT ( 'NONE',  ( -2.699999999999995737, 0.000000000000000000, -20.30000000000000071 ) ) ;
#6866=CIRCLE ( 'NONE', #14582, 21.02499999999999503 ) ;
#6909=ORIENTED_EDGE ( 'NONE', *, *, #16827, .F. ) ;
#6920=CIRCLE ( 'NONE', #12372, 21.02499999999999503 ) ;
#6944=EDGE_CURVE ( 'NONE', #13630, #3512, #11242, .T. ) ;
#6983=EDGE_CURVE ( 'NONE', #15719, #7318, #14016, .T. ) ;
#6996=EDGE_LOOP ( 'NONE', ( #945, #2595, #23581, #9753 ) ) ;
#7045=ORIENTED_EDGE ( 'NONE', *, *, #10974, .F. ) ;
#7094=TOROIDAL_SURFACE ( 'NONE', #12173, 22.50000000000000000, 1.500000000000000444 ) ;
#7132=DIRECTION ( 'NONE',  ( 0.000000000000000000, 0.000000000000000000, 1.000000000000000000 ) ) ;
#7139=TOROIDAL_SURFACE ( 'NONE', #3658, 24.69999999999999929, 0.3000000000000007661 ) ;
#7143=FACE_OUTER_BOUND ( 'NONE', #2052, .T. ) ;
#7149=ORIENTED_EDGE ( 'NONE', *, *, #14358, .T. ) ;
#7152=CARTESIAN_POINT ( 'NONE',  ( -1.118033988749894458, 0.000000000000000000, 0.000000000000000000 ) ) ;
#7165=ORIENTED_EDGE ( 'NONE', *, *, #7872, .F. ) ;
#7191=CARTESIAN_POINT ( 'NONE',  ( 3.000000000000002665, 0.000000000000000000, 0.000000000000000000 ) ) ;
#7214=AXIS2_PLACEMENT_3D ( 'NONE', #12353, #21472, #19661 ) ;
#7318=VERTEX_POINT ( 'NONE', #16419 ) ;
#7323=CARTESIAN_POINT ( 'NONE',  ( 2.700000000000001510, 0.000000000000000000, -24.69999999999999929 ) ) ;
#7353=ORIENTED_EDGE ( 'NONE', *, *, #16566, .T. ) ;
#7356=TOROIDAL_SURFACE ( 'NONE', #10854, 24.69999999999999929, 0.3000000000000007661 ) ;
#7461=DIRECTION ( 'NONE',  ( 0.000000000000000000, 0.000000000000000000, -1.000000000000000000 ) ) ;
#7471=ORIENTED_EDGE ( 'NONE', *, *, #22339, .F. ) ;
#7686=MECHANICAL_DESIGN_GEOMETRIC_PRESENTATION_REPRESENTATION('',(#3437),#8855);
#7712=LINE ( 'NONE', #22542, #8515 ) ;
#7716=EDGE_CURVE ( 'NONE', #20294, #13434, #3211, .T. ) ;
#7750=ORIENTED_EDGE ( 'NONE', *, *, #13281, .F. ) ;
#7755=ORIENTED_EDGE ( 'NONE', *, *, #21249, .T. ) ;
#7792=CYLINDRICAL_SURFACE ( 'NONE', #22138, 19.99999999999999289 ) ;
#7834=FACE_BOUND ( 'NONE', #3099, .T. ) ;
#7836=ADVANCED_FACE ( 'NONE', ( #2362 ), #9627, .F. ) ;
#7841=EDGE_CURVE ( 'NONE', #8826, #15719, #449, .T. ) ;
#7872=EDGE_CURVE ( 'NONE', #18148, #17543, #5525, .T. ) ;
#7886=CIRCLE ( 'NONE', #8669, 24.69999999999999929 ) ;
#7922=ORIENTED_EDGE ( 'NONE', *, *, #4721, .T. ) ;
#7928=EDGE_LOOP ( 'NONE', ( #3032, #4402, #9014, #8821 ) ) ;
#7937=FACE_OUTER_BOUND ( 'NONE', #9600, .T. ) ;
#7957=AXIS2_PLACEMENT_3D ( 'NONE', #21872, #9216, #5343 ) ;
#7974=FACE_OUTER_BOUND ( 'NONE', #6735, .T. ) ;
#8010=EDGE_CURVE ( 'NONE', #9561, #17846, #3186, .T. ) ;
#8038=ORIENTED_EDGE ( 'NONE', *, *, #17016, .T. ) ;
#8046=AXIS2_PLACEMENT_3D ( 'NONE', #685, #4183, #19026 ) ;
#8047=EDGE_CURVE ( 'NONE', #2929, #22100, #15549, .T. ) ;
#8068=AXIS2_PLACEMENT_3D ( 'NONE', #7191, #1750, #2110 ) ;
#8086=AXIS2_PLACEMENT_3D ( 'NONE', #1377, #19368, #2827 ) ;
#8145=ORIENTED_EDGE ( 'NONE', *, *, #5155, .F. ) ;
#8177=CARTESIAN_POINT ( 'NONE',  ( -2.700000000000001066, 0.000000000000000000, 0.000000000000000000 ) ) ;
#8191=ADVANCED_FACE ( 'NONE', ( #20410 ), #16568, .F. ) ;
#8203=AXIS2_PLACEMENT_3D ( 'NONE', #5645, #18659, #14598 ) ;
#8221=DIRECTION ( 'NONE',  ( 1.000000000000000000, 0.000000000000000000, 0.000000000000000000 ) ) ;
#8282=DIRECTION ( 'NONE',  ( 1.000000000000000000, 0.000000000000000000, 0.000000000000000000 ) ) ;
#8284=DIRECTION ( 'NONE',  ( 1.000000000000000000, 0.000000000000000000, 0.000000000000000000 ) ) ;
#8409=CARTESIAN_POINT ( 'NONE',  ( 2.999999999999995559, 0.000000000000000000, 0.000000000000000000 ) ) ;
#8412=CARTESIAN_POINT ( 'NONE',  ( 0.2727178028658734932, 0.000000000000000000, 0.000000000000000000 ) ) ;
#8515=VECTOR ( 'NONE', #13195, 1000.000000000000000 ) ;
#8544=EDGE_CURVE ( 'NONE', #5300, #15719, #10716, .T. ) ;
#8573=PLANE ( 'NONE',  #22105 ) ;
#8611=EDGE_CURVE ( 'NONE', #20731, #8622, #16870, .T. ) ;
#8622=VERTEX_POINT ( 'NONE', #20614 ) ;
#8645=ADVANCED_FACE ( 'NONE', ( #11483, #7834 ), #9670, .T. ) ;
#8656=VERTEX_POINT ( 'NONE', #22550 ) ;
#8661=DIRECTION ( 'NONE',  ( 1.000000000000000000, 0.000000000000000000, 0.000000000000000000 ) ) ;
#8669=AXIS2_PLACEMENT_3D ( 'NONE', #664, #6098, #15298 ) ;
#8672=ORIENTED_EDGE ( 'NONE', *, *, #22375, .F. ) ;
#8719=EDGE_CURVE ( 'NONE', #23365, #17297, #1805, .T. ) ;
#8728=ORIENTED_EDGE ( 'NONE', *, *, #9758, .T. ) ;
#8737=DIRECTION ( 'NONE',  ( -1.000000000000000000, -0.000000000000000000, -0.000000000000000000 ) ) ;
#8763=CYLINDRICAL_SURFACE ( 'NONE', #22693, 21.02499999999999503 ) ;
#8810=ORIENTED_EDGE ( 'NONE', *, *, #17016, .F. ) ;
#8821=ORIENTED_EDGE ( 'NONE', *, *, #12306, .F. ) ;
#8826=VERTEX_POINT ( 'NONE', #23265 ) ;
#8855=( GEOMETRIC_REPRESENTATION_CONTEXT ( 3 ) GLOBAL_UNCERTAINTY_ASSIGNED_CONTEXT ( ( #2685 ) ) GLOBAL_UNIT_ASSIGNED_CONTEXT ( ( #414, #19335, #6784 ) ) REPRESENTATION_CONTEXT ( 'NONE', 'WORKASPACE' ) );
#8861=DIRECTION ( 'NONE',  ( 0.000000000000000000, 0.000000000000000000, -1.000000000000000000 ) ) ;
#8900=EDGE_CURVE ( 'NONE', #20731, #17846, #5679, .T. ) ;
#8921=FACE_OUTER_BOUND ( 'NONE', #11520, .T. ) ;
#8928=EDGE_LOOP ( 'NONE', ( #13313, #14377, #919, #8038 ) ) ;
#9014=ORIENTED_EDGE ( 'NONE', *, *, #23444, .T. ) ;
#9017=CIRCLE ( 'NONE', #13678, 24.69999999999999929 ) ;
#9044=DIRECTION ( 'NONE',  ( 1.000000000000000000, 0.000000000000000000, 0.000000000000000000 ) ) ;
#9095=ORIENTED_EDGE ( 'NONE', *, *, #6944, .T. ) ;
#9185=AXIS2_PLACEMENT_3D ( 'NONE', #12469, #6743, #1418 ) ;
#9208=PRESENTATION_STYLE_ASSIGNMENT (( #1697 ) ) ;
#9216=DIRECTION ( 'NONE',  ( 1.000000000000000000, 0.000000000000000000, 0.000000000000000000 ) ) ;
#9240=CIRCLE ( 'NONE', #23499, 21.50000000000000000 ) ;
#9247=FACE_OUTER_BOUND ( 'NONE', #14196, .T. ) ;
#9278=( GEOMETRIC_REPRESENTATION_CONTEXT ( 3 ) GLOBAL_UNCERTAINTY_ASSIGNED_CONTEXT ( ( #11609 ) ) GLOBAL_UNIT_ASSIGNED_CONTEXT ( ( #3875, #18243, #3389 ) ) REPRESENTATION_CONTEXT ( 'NONE', 'WORKASPACE' ) );
#9376=ORIENTED_EDGE ( 'NONE', *, *, #2891, .T. ) ;
#9390=ORIENTED_EDGE ( 'NONE', *, *, #13505, .T. ) ;
#9454=DIRECTION ( 'NONE',  ( 0.000000000000000000, 0.000000000000000000, -1.000000000000000000 ) ) ;
#9473=CARTESIAN_POINT ( 'NONE',  ( 0.000000000000000000, 0.000000000000000000, 0.000000000000000000 ) ) ;
#9531=ORIENTED_EDGE ( 'NONE', *, *, #5830, .T. ) ;
#9561=VERTEX_POINT ( 'NONE', #12153 ) ;
#9600=EDGE_LOOP ( 'NONE', ( #12740, #9531, #1606, #16502 ) ) ;
#9602=DIRECTION ( 'NONE',  ( 1.000000000000000000, 0.000000000000000000, 0.000000000000000000 ) ) ;
#9627=CYLINDRICAL_SURFACE ( 'NONE', #19780, 23.50000000000000000 ) ;
#9630=PRODUCT_DEFINITION ( 'UNKNOWN', '', #1160, #12956 ) ;
#9657=ORIENTED_EDGE ( 'NONE', *, *, #23444, .F. ) ;
#9661=VECTOR ( 'NONE', #8661, 1000.000000000000000 ) ;
#9663=AXIS2_PLACEMENT_3D ( 'NONE', #14532, #19827, #21868 ) ;
#9670=PLANE ( 'NONE',  #23419 ) ;
#9687=CYLINDRICAL_SURFACE ( 'NONE', #13153, 25.00000000000000000 ) ;
#9691=DIRECTION ( 'NONE',  ( 0.000000000000000000, 0.000000000000000000, -1.000000000000000000 ) ) ;
#9722=DIRECTION ( 'NONE',  ( 1.000000000000000000, 0.000000000000000000, 0.000000000000000000 ) ) ;
#9727=ADVANCED_FACE ( 'NONE', ( #7143 ), #5460, .F. ) ;
#9742=DIRECTION ( 'NONE',  ( 0.000000000000000000, 0.000000000000000000, -1.000000000000000000 ) ) ;
#9746=CARTESIAN_POINT ( 'NONE',  ( -20.63749999999999929, 2.449293598294705724E-15, 19.99999999999999289 ) ) ;
#9752=AXIS2_PLACEMENT_3D ( 'NONE', #9802, #4230, #9691 ) ;
#9753=ORIENTED_EDGE ( 'NONE', *, *, #20698, .F. ) ;
#9758=EDGE_CURVE ( 'NONE', #8622, #9561, #16974, .T. ) ;
#9793=ORIENTED_EDGE ( 'NONE', *, *, #14358, .F. ) ;
#9802=CARTESIAN_POINT ( 'NONE',  ( 2.700000000000001066, 0.000000000000000000, 0.000000000000000000 ) ) ;
#9821=CARTESIAN_POINT ( 'NONE',  ( 3.000000000000002665, 0.000000000000000000, 0.000000000000000000 ) ) ;
#9982=CARTESIAN_POINT ( 'NONE',  ( -20.63749999999999929, 0.000000000000000000, -21.50000000000000000 ) ) ;
#10111=CARTESIAN_POINT ( 'NONE',  ( -3.000000000000002665, 0.000000000000000000, 0.000000000000000000 ) ) ;
#10141=ORIENTED_EDGE ( 'NONE', *, *, #2891, .F. ) ;
#10187=CARTESIAN_POINT ( 'NONE',  ( 2.699999999999995737, 0.000000000000000000, 0.000000000000000000 ) ) ;
#10233=AXIS2_PLACEMENT_3D ( 'NONE', #12805, #16483, #4024 ) ;
#10291=CIRCLE ( 'NONE', #6813, 21.50000000000000000 ) ;
#10301=DIRECTION ( 'NONE',  ( 1.000000000000000000, 0.000000000000000000, 0.000000000000000000 ) ) ;
#10303=DIRECTION ( 'NONE',  ( -0.000000000000000000, 1.000000000000000000, 1.224646799147353207E-16 ) ) ;
#10309=ORIENTED_EDGE ( 'NONE', *, *, #2730, .T. ) ;
#10349=ORIENTED_EDGE ( 'NONE', *, *, #15251, .T. ) ;
#10405=LINE ( 'NONE', #842, #12022 ) ;
#10603=VECTOR ( 'NONE', #2616, 1000.000000000000000 ) ;
#10614=LINE ( 'NONE', #17954, #9661 ) ;
#10647=EDGE_LOOP ( 'NONE', ( #17312, #14255, #17799, #16736 ) ) ;
#10652=DIRECTION ( 'NONE',  ( 0.000000000000000000, -1.000000000000000000, 0.000000000000000000 ) ) ;
#10689=DIRECTION ( 'NONE',  ( 0.000000000000000000, -1.000000000000000000, 0.000000000000000000 ) ) ;
#10716=CIRCLE ( 'NONE', #2573, 0.3000000000000051514 ) ;
#10730=EDGE_LOOP ( 'NONE', ( #8672, #7149, #4717, #9376 ) ) ;
#10736=DIRECTION ( 'NONE',  ( 0.000000000000000000, -1.000000000000000000, 0.000000000000000000 ) ) ;
#10814=AXIS2_PLACEMENT_3D ( 'NONE', #8409, #15792, #23137 ) ;
#10846=CYLINDRICAL_SURFACE ( 'NONE', #12023, 21.02499999999999503 ) ;
#10854=AXIS2_PLACEMENT_3D ( 'NONE', #22740, #15876, #877 ) ;
#10930=CARTESIAN_POINT ( 'NONE',  ( -2.700000000000001066, 0.000000000000000000, -25.00000000000000000 ) ) ;
#10947=CARTESIAN_POINT ( 'NONE',  ( -2.999999999999995559, 2.632990618166809235E-15, 21.50000000000000000 ) ) ;
#10974=EDGE_CURVE ( 'NONE', #17846, #9561, #15581, .T. ) ;
#11019=CARTESIAN_POINT ( 'NONE',  ( 2.699999999999997513, 0.000000000000000000, 0.000000000000000000 ) ) ;
#11034=EDGE_LOOP ( 'NONE', ( #19208, #13941 ) ) ;
#11049=AXIS2_PLACEMENT_3D ( 'NONE', #11139, #18464, #1923 ) ;
#11118=AXIS2_PLACEMENT_3D ( 'NONE', #11559, #9602, #22853 ) ;
#11122=ORIENTED_EDGE ( 'NONE', *, *, #22293, .F. ) ;
#11132=AXIS2_PLACEMENT_3D ( 'NONE', #23353, #13988, #19728 ) ;
#11139=CARTESIAN_POINT ( 'NONE',  ( -2.699999999999995737, 2.486033002269127373E-15, 20.30000000000000071 ) ) ;
#11157=ORIENTED_EDGE ( 'NONE', *, *, #8544, .T. ) ;
#11161=EDGE_LOOP ( 'NONE', ( #16441, #7922, #11468, #11122 ) ) ;
#11200=CYLINDRICAL_SURFACE ( 'NONE', #20830, 21.50000000000000000 ) ;
#11210=AXIS2_PLACEMENT_3D ( 'NONE', #9473, #14914, #3769 ) ;
#11242=LINE ( 'NONE', #5419, #17067 ) ;
#11297=ORIENTED_EDGE ( 'NONE', *, *, #22293, .T. ) ;
#11363=VERTEX_POINT ( 'NONE', #18813 ) ;
#11468=ORIENTED_EDGE ( 'NONE', *, *, #8719, .F. ) ;
#11483=FACE_OUTER_BOUND ( 'NONE', #607, .T. ) ;
#11515=AXIS2_PLACEMENT_3D ( 'NONE', #15245, #5925, #18592 ) ;
#11520=EDGE_LOOP ( 'NONE', ( #956, #9390, #17150, #13613 ) ) ;
#11542=ADVANCED_FACE ( 'NONE', ( #21481, #23042 ), #8573, .T. ) ;
#11559=CARTESIAN_POINT ( 'NONE',  ( 3.000000000000002665, 0.000000000000000000, 0.000000000000000000 ) ) ;
#11574=EDGE_LOOP ( 'NONE', ( #23488, #5700, #16586, #7165 ) ) ;
#11609=UNCERTAINTY_MEASURE_WITH_UNIT (LENGTH_MEASURE( 1.000000000000000082E-05 ), #3875, 'distance_accuracy_value', 'NONE');
#11629=ORIENTED_EDGE ( 'NONE', *, *, #8544, .F. ) ;
#11742=APPLICATION_CONTEXT ( 'automotive_design' ) ;
#11857=DIRECTION ( 'NONE',  ( 1.000000000000000000, 0.000000000000000000, 0.000000000000000000 ) ) ;
#11888=PLANE ( 'NONE',  #2603 ) ;
#11904=DIRECTION ( 'NONE',  ( 1.000000000000000000, 0.000000000000000000, 0.000000000000000000 ) ) ;
#11907=DIRECTION ( 'NONE',  ( 0.000000000000000000, 0.000000000000000000, -1.000000000000000000 ) ) ;
#11959=( GEOMETRIC_REPRESENTATION_CONTEXT ( 3 ) GLOBAL_UNCERTAINTY_ASSIGNED_CONTEXT ( ( #2383 ) ) GLOBAL_UNIT_ASSIGNED_CONTEXT ( ( #20647, #17050, #19193 ) ) REPRESENTATION_CONTEXT ( 'NONE', 'WORKASPACE' ) );
#11981=EDGE_LOOP ( 'NONE', ( #12732, #16545 ) ) ;
#11996=CARTESIAN_POINT ( 'NONE',  ( -1.118033988749894458, 2.632990618166809235E-15, 21.50000000000000000 ) ) ;
#11998=EDGE_CURVE ( 'NONE', #11363, #8656, #6480, .T. ) ;
#12022=VECTOR ( 'NONE', #8221, 1000.000000000000000 ) ;
#12023=AXIS2_PLACEMENT_3D ( 'NONE', #16610, #1620, #23710 ) ;
#12031=DIRECTION ( 'NONE',  ( 0.000000000000000000, 0.000000000000000000, -1.000000000000000000 ) ) ;
#12044=DIRECTION ( 'NONE',  ( 0.000000000000000000, 0.000000000000000000, -1.000000000000000000 ) ) ;
#12105=DIRECTION ( 'NONE',  ( 1.000000000000000000, 0.000000000000000000, 0.000000000000000000 ) ) ;
#12116=ORIENTED_EDGE ( 'NONE', *, *, #9758, .F. ) ;
#12153=CARTESIAN_POINT ( 'NONE',  ( -2.700000000000001066, 3.061616997868383043E-15, 25.00000000000000000 ) ) ;
#12173=AXIS2_PLACEMENT_3D ( 'NONE', #4298, #17562, #21311 ) ;
#12214=CLOSED_SHELL ( 'NONE', ( #15414, #1770, #5040, #18069, #8191, #13066, #21544, #12279, #21530, #15237, #21141, #1728, #21745, #15173, #16639, #18171, #12609, #1916, #22969, #15847, #6293, #7836, #9727, #4465, #5637, #4259, #8645, #11542 ) ) ;
#12253=DIRECTION ( 'NONE',  ( 0.000000000000000000, 0.000000000000000000, -1.000000000000000000 ) ) ;
#12278=ORIENTED_EDGE ( 'NONE', *, *, #20313, .T. ) ;
#12279=ADVANCED_FACE ( 'NONE', ( #441 ), #7792, .F. ) ;
#12304=AXIS2_PLACEMENT_3D ( 'NONE', #5939, #22473, #2062 ) ;
#12306=EDGE_CURVE ( 'NONE', #15926, #5940, #7886, .T. ) ;
#12353=CARTESIAN_POINT ( 'NONE',  ( -2.699999999999997513, 0.000000000000000000, 0.000000000000000000 ) ) ;
#12372=AXIS2_PLACEMENT_3D ( 'NONE', #8412, #687, #6475 ) ;
#12394=FACE_OUTER_BOUND ( 'NONE', #4652, .T. ) ;
#12423=DIRECTION ( 'NONE',  ( 1.000000000000000000, 0.000000000000000000, 0.000000000000000000 ) ) ;
#12469=CARTESIAN_POINT ( 'NONE',  ( -2.699999999999997513, 0.000000000000000000, 0.000000000000000000 ) ) ;
#12478=EDGE_CURVE ( 'NONE', #8622, #20731, #9017, .T. ) ;
#12512=ORIENTED_EDGE ( 'NONE', *, *, #13672, .F. ) ;
#12529=CARTESIAN_POINT ( 'NONE',  ( -2.700000000000001510, 0.000000000000000000, 0.000000000000000000 ) ) ;
#12540=DIRECTION ( 'NONE',  ( 1.000000000000000000, 0.000000000000000000, 0.000000000000000000 ) ) ;
#12609=ADVANCED_FACE ( 'NONE', ( #12394 ), #2042, .T. ) ;
#12611=AXIS2_PLACEMENT_3D ( 'NONE', #12529, #12423, #1371 ) ;
#12635=EDGE_LOOP ( 'NONE', ( #22358, #15946, #18213, #20719 ) ) ;
#12665=CYLINDRICAL_SURFACE ( 'NONE', #6107, 19.99999999999999289 ) ;
#12679=DIRECTION ( 'NONE',  ( 0.000000000000000000, 0.000000000000000000, 1.000000000000000000 ) ) ;
#12682=CIRCLE ( 'NONE', #11118, 20.30000000000000071 ) ;
#12691=CARTESIAN_POINT ( 'NONE',  ( -2.700000000000001510, 0.000000000000000000, -24.69999999999999929 ) ) ;
#12732=ORIENTED_EDGE ( 'NONE', *, *, #22339, .T. ) ;
#12740=ORIENTED_EDGE ( 'NONE', *, *, #10974, .T. ) ;
#12752=FILL_AREA_STYLE ('',( #16569 ) ) ;
#12805=CARTESIAN_POINT ( 'NONE',  ( -2.700000000000001066, 0.000000000000000000, 0.000000000000000000 ) ) ;
#12868=ORIENTED_EDGE ( 'NONE', *, *, #15548, .F. ) ;
#12881=ORIENTED_EDGE ( 'NONE', *, *, #11998, .F. ) ;
#12903=DIRECTION ( 'NONE',  ( 0.000000000000000000, 0.000000000000000000, -1.000000000000000000 ) ) ;
#12956=PRODUCT_DEFINITION_CONTEXT ( 'detailed design', #11742, 'design' ) ;
#13005=CARTESIAN_POINT ( 'NONE',  ( 2.999999999999995559, 0.000000000000000000, -21.02499999999999858 ) ) ;
#13011=FACE_OUTER_BOUND ( 'NONE', #11161, .T. ) ;
#13066=ADVANCED_FACE ( 'NONE', ( #15769 ), #7094, .T. ) ;
#13121=CIRCLE ( 'NONE', #22703, 25.00000000000000000 ) ;
#13153=AXIS2_PLACEMENT_3D ( 'NONE', #4090, #720, #15354 ) ;
#13167=CARTESIAN_POINT ( 'NONE',  ( -1.118033988749894458, 0.000000000000000000, -21.50000000000000000 ) ) ;
#13170=EDGE_LOOP ( 'NONE', ( #7353, #5253 ) ) ;
#13195=DIRECTION ( 'NONE',  ( 1.000000000000000000, 0.000000000000000000, 0.000000000000000000 ) ) ;
#13224=DIRECTION ( 'NONE',  ( 0.000000000000000000, 0.000000000000000000, -1.000000000000000000 ) ) ;
#13276=VECTOR ( 'NONE', #6110, 1000.000000000000000 ) ;
#13281=EDGE_CURVE ( 'NONE', #18427, #13434, #5187, .T. ) ;
#13290=DIRECTION ( 'NONE',  ( 0.000000000000000000, 0.000000000000000000, -1.000000000000000000 ) ) ;
#13313=ORIENTED_EDGE ( 'NONE', *, *, #7841, .F. ) ;
#13386=DIRECTION ( 'NONE',  ( 0.000000000000000000, 0.000000000000000000, -1.000000000000000000 ) ) ;
#13407=FACE_OUTER_BOUND ( 'NONE', #4342, .T. ) ;
#13434=VERTEX_POINT ( 'NONE', #13005 ) ;
#13505=EDGE_CURVE ( 'NONE', #23227, #22100, #4574, .T. ) ;
#13527=FACE_OUTER_BOUND ( 'NONE', #12635, .T. ) ;
#13566=AXIS2_PLACEMENT_3D ( 'NONE', #3775, #9722, #6077 ) ;
#13613=ORIENTED_EDGE ( 'NONE', *, *, #3938, .T. ) ;
#13630=VERTEX_POINT ( 'NONE', #22602 ) ;
#13672=EDGE_CURVE ( 'NONE', #22100, #23227, #15400, .T. ) ;
#13678=AXIS2_PLACEMENT_3D ( 'NONE', #2438, #11904, #19211 ) ;
#13709=FACE_OUTER_BOUND ( 'NONE', #23322, .T. ) ;
#13744=ORIENTED_EDGE ( 'NONE', *, *, #3507, .T. ) ;
#13834=CARTESIAN_POINT ( 'NONE',  ( 0.000000000000000000, 2.755455298081544778E-15, -22.50000000000000000 ) ) ;
#13838=FACE_OUTER_BOUND ( 'NONE', #21495, .T. ) ;
#13851=AXIS2_PLACEMENT_3D ( 'NONE', #10111, #17455, #6229 ) ;
#13928=CARTESIAN_POINT ( 'NONE',  ( -3.000000000000001332, 23.97500000000000142, 0.000000000000000000 ) ) ;
#13941=ORIENTED_EDGE ( 'NONE', *, *, #17653, .F. ) ;
#13964=CARTESIAN_POINT ( 'NONE',  ( -2.699999999999995737, 0.000000000000000000, 0.000000000000000000 ) ) ;
#13982=EDGE_LOOP ( 'NONE', ( #18636, #12278, #17070, #6513 ) ) ;
#13988=DIRECTION ( 'NONE',  ( -0.000000000000000000, 1.000000000000000000, 1.224646799147353207E-16 ) ) ;
#14002=CARTESIAN_POINT ( 'NONE',  ( 3.000000000000002665, 2.877919977996280320E-15, 23.50000000000000000 ) ) ;
#14009=CARTESIAN_POINT ( 'NONE',  ( -0.2727178028658734932, 0.000000000000000000, 23.97500000000000497 ) ) ;
#14016=CIRCLE ( 'NONE', #8203, 19.99999999999998934 ) ;
#14042=ORIENTED_EDGE ( 'NONE', *, *, #15251, .F. ) ;
#14097=CARTESIAN_POINT ( 'NONE',  ( 2.999999999999995559, 0.000000000000000000, 0.000000000000000000 ) ) ;
#14113=DIRECTION ( 'NONE',  ( 1.000000000000000000, 0.000000000000000000, 0.000000000000000000 ) ) ;
#14174=CARTESIAN_POINT ( 'NONE',  ( 2.699999999999995737, 0.000000000000000000, 0.000000000000000000 ) ) ;
#14196=EDGE_LOOP ( 'NONE', ( #8145, #9793, #16814, #7750 ) ) ;
#14255=ORIENTED_EDGE ( 'NONE', *, *, #7841, .T. ) ;
#14272=LINE ( 'NONE', #20330, #21022 ) ;
#14308=VERTEX_POINT ( 'NONE', #22891 ) ;
#14358=EDGE_CURVE ( 'NONE', #20294, #22350, #6920, .T. ) ;
#14377=ORIENTED_EDGE ( 'NONE', *, *, #15780, .F. ) ;
#14445=ORIENTED_EDGE ( 'NONE', *, *, #17653, .T. ) ;
#14493=ORIENTED_EDGE ( 'NONE', *, *, #15516, .T. ) ;
#14528=SURFACE_SIDE_STYLE ('',( #23678 ) ) ;
#14532=CARTESIAN_POINT ( 'NONE',  ( -2.700000000000001510, 3.024877593893962577E-15, 24.69999999999999929 ) ) ;
#14544=ORIENTED_EDGE ( 'NONE', *, *, #8900, .F. ) ;
#14582=AXIS2_PLACEMENT_3D ( 'NONE', #16448, #8737, #15986 ) ;
#14595=AXIS2_PLACEMENT_3D ( 'NONE', #13834, #10303, #15974 ) ;
#14598=DIRECTION ( 'NONE',  ( 0.000000000000000000, 0.000000000000000000, -1.000000000000000000 ) ) ;
#14609=SHAPE_DEFINITION_REPRESENTATION ( #3420, #14711 ) ;
#14629=TOROIDAL_SURFACE ( 'NONE', #738, 20.30000000000000071, 0.3000000000000059841 ) ;
#14661=CYLINDRICAL_SURFACE ( 'NONE', #7957, 21.50000000000000000 ) ;
#14711=SHAPE_REPRESENTATION ( 'angular contact ball bearing_68_iso_ISO 15 ABB - 1740 - 38,SI,NC,38_68', ( #11210 ), #9278 ) ;
#14736=PRODUCT_CONTEXT ( 'NONE', #2750, 'mechanical' ) ;
#14914=DIRECTION ( 'NONE',  ( 0.000000000000000000, 0.000000000000000000, 1.000000000000000000 ) ) ;
#14984=ORIENTED_EDGE ( 'NONE', *, *, #12478, .F. ) ;
#15095=FACE_OUTER_BOUND ( 'NONE', #8928, .T. ) ;
#15173=ADVANCED_FACE ( 'NONE', ( #9247 ), #10846, .T. ) ;
#15177=CARTESIAN_POINT ( 'NONE',  ( -20.63749999999999929, 0.000000000000000000, 0.000000000000000000 ) ) ;
#15187=VECTOR ( 'NONE', #17816, 1000.000000000000000 ) ;
#15237=ADVANCED_FACE ( 'NONE', ( #13011 ), #11200, .T. ) ;
#15245=CARTESIAN_POINT ( 'NONE',  ( 0.000000000000000000, 0.000000000000000000, 0.000000000000000000 ) ) ;
#15251=EDGE_CURVE ( 'NONE', #8656, #3512, #1927, .T. ) ;
#15298=DIRECTION ( 'NONE',  ( 0.000000000000000000, 0.000000000000000000, -1.000000000000000000 ) ) ;
#15306=DIRECTION ( 'NONE',  ( 1.000000000000000000, 0.000000000000000000, 0.000000000000000000 ) ) ;
#15354=DIRECTION ( 'NONE',  ( 0.000000000000000000, 0.000000000000000000, -1.000000000000000000 ) ) ;
#15369=DIRECTION ( 'NONE',  ( 1.000000000000000000, 0.000000000000000000, 0.000000000000000000 ) ) ;
#15391=EDGE_LOOP ( 'NONE', ( #10141, #9095, #5070, #12881 ) ) ;
#15400=CIRCLE ( 'NONE', #1866, 23.97500000000000497 ) ;
#15414=ADVANCED_FACE ( 'NONE', ( #2704 ), #7356, .T. ) ;
#15516=EDGE_CURVE ( 'NONE', #22350, #20294, #6866, .T. ) ;
#15542=DIRECTION ( 'NONE',  ( 1.000000000000000000, 0.000000000000000000, 0.000000000000000000 ) ) ;
#15548=EDGE_CURVE ( 'NONE', #5262, #7318, #5689, .T. ) ;
#15549=LINE ( 'NONE', #1151, #15187 ) ;
#15574=CARTESIAN_POINT ( 'NONE',  ( -0.2727178028658734932, 2.936090700955779752E-15, -23.97500000000000497 ) ) ;
#15581=CIRCLE ( 'NONE', #10233, 25.00000000000000000 ) ;
#15629=VECTOR ( 'NONE', #6604, 1000.000000000000000 ) ;
#15691=EDGE_LOOP ( 'NONE', ( #21086, #14984 ) ) ;
#15719=VERTEX_POINT ( 'NONE', #19658 ) ;
#15769=FACE_OUTER_BOUND ( 'NONE', #13982, .T. ) ;
#15780=EDGE_CURVE ( 'NONE', #14308, #8826, #4145, .T. ) ;
#15792=DIRECTION ( 'NONE',  ( 1.000000000000000000, 0.000000000000000000, 0.000000000000000000 ) ) ;
#15847=ADVANCED_FACE ( 'NONE', ( #17290, #4481 ), #11888, .T. ) ;
#15865=DIRECTION ( 'NONE',  ( 0.000000000000000000, 0.000000000000000000, -1.000000000000000000 ) ) ;
#15876=DIRECTION ( 'NONE',  ( 1.000000000000000000, 0.000000000000000000, 0.000000000000000000 ) ) ;
#15901=ORIENTED_EDGE ( 'NONE', *, *, #3938, .F. ) ;
#15926=VERTEX_POINT ( 'NONE', #3472 ) ;
#15932=CARTESIAN_POINT ( 'NONE',  ( -2.999999999999996003, 21.50000000000000000, 0.000000000000000000 ) ) ;
#15946=ORIENTED_EDGE ( 'NONE', *, *, #5155, .T. ) ;
#15974=DIRECTION ( 'NONE',  ( 0.000000000000000000, -1.224646799147351975E-16, 1.000000000000000000 ) ) ;
#15986=DIRECTION ( 'NONE',  ( 0.000000000000000000, 0.000000000000000000, 1.000000000000000000 ) ) ;
#15999=EDGE_LOOP ( 'NONE', ( #6909, #338 ) ) ;
#16008=DIRECTION ( 'NONE',  ( 0.000000000000000000, 0.000000000000000000, -1.000000000000000000 ) ) ;
#16148=AXIS2_PLACEMENT_3D ( 'NONE', #18223, #10652, #17990 ) ;
#16190=TOROIDAL_SURFACE ( 'NONE', #4986, 20.30000000000000071, 0.3000000000000059841 ) ;
#16337=DIRECTION ( 'NONE',  ( 0.000000000000000000, 0.000000000000000000, -1.000000000000000000 ) ) ;
#16419=CARTESIAN_POINT ( 'NONE',  ( 2.699999999999997513, 0.000000000000000000, -19.99999999999998934 ) ) ;
#16441=ORIENTED_EDGE ( 'NONE', *, *, #16827, .T. ) ;
#16448=CARTESIAN_POINT ( 'NONE',  ( 0.2727178028658734932, 0.000000000000000000, 0.000000000000000000 ) ) ;
#16483=DIRECTION ( 'NONE',  ( 1.000000000000000000, 0.000000000000000000, 0.000000000000000000 ) ) ;
#16502=ORIENTED_EDGE ( 'NONE', *, *, #19732, .F. ) ;
#16506=ORIENTED_EDGE ( 'NONE', *, *, #6400, .T. ) ;
#16515=AXIS2_PLACEMENT_3D ( 'NONE', #5774, #20597, #13290 ) ;
#16545=ORIENTED_EDGE ( 'NONE', *, *, #2804, .T. ) ;
#16566=EDGE_CURVE ( 'NONE', #17543, #18148, #22979, .T. ) ;
#16568=CYLINDRICAL_SURFACE ( 'NONE', #21856, 23.50000000000000000 ) ;
#16569=FILL_AREA_STYLE_COLOUR ( '', #4968 ) ;
#16586=ORIENTED_EDGE ( 'NONE', *, *, #20698, .T. ) ;
#16610=CARTESIAN_POINT ( 'NONE',  ( -20.63749999999999929, 0.000000000000000000, 0.000000000000000000 ) ) ;
#16639=ADVANCED_FACE ( 'NONE', ( #879 ), #14661, .T. ) ;
#16699=ORIENTED_EDGE ( 'NONE', *, *, #11998, .T. ) ;
#16736=ORIENTED_EDGE ( 'NONE', *, *, #5943, .F. ) ;
#16814=ORIENTED_EDGE ( 'NONE', *, *, #7716, .T. ) ;
#16827=EDGE_CURVE ( 'NONE', #22490, #21286, #10291, .T. ) ;
#16855=CARTESIAN_POINT ( 'NONE',  ( -2.999999999999995559, 0.000000000000000000, 0.000000000000000000 ) ) ;
#16870=CIRCLE ( 'NONE', #1036, 24.69999999999999929 ) ;
#16888=DIRECTION ( 'NONE',  ( 1.000000000000000000, 0.000000000000000000, 0.000000000000000000 ) ) ;
#16894=CIRCLE ( 'NONE', #11132, 1.500000000000001332 ) ;
#16895=ORIENTED_EDGE ( 'NONE', *, *, #8010, .F. ) ;
#16944=CARTESIAN_POINT ( 'NONE',  ( 3.000000000000002220, 0.000000000000000000, -20.30000000000000071 ) ) ;
#16974=CIRCLE ( 'NONE', #9663, 0.3000000000000016542 ) ;
#17016=EDGE_CURVE ( 'NONE', #7318, #15719, #5279, .T. ) ;
#17023=FACE_OUTER_BOUND ( 'NONE', #11574, .T. ) ;
#17050=( NAMED_UNIT ( * ) PLANE_ANGLE_UNIT ( ) SI_UNIT ( $, .RADIAN. ) );
#17067=VECTOR ( 'NONE', #9044, 1000.000000000000000 ) ;
#17069=CARTESIAN_POINT ( 'NONE',  ( -0.2727178028658734932, 0.000000000000000000, 0.000000000000000000 ) ) ;
#17070=ORIENTED_EDGE ( 'NONE', *, *, #8719, .T. ) ;
#17103=VECTOR ( 'NONE', #3332, 1000.000000000000000 ) ;
#17150=ORIENTED_EDGE ( 'NONE', *, *, #22859, .T. ) ;
#17213=ORIENTED_EDGE ( 'NONE', *, *, #650, .T. ) ;
#17290=FACE_BOUND ( 'NONE', #13170, .T. ) ;
#17297=VERTEX_POINT ( 'NONE', #11996 ) ;
#17312=ORIENTED_EDGE ( 'NONE', *, *, #17469, .F. ) ;
#17446=EDGE_LOOP ( 'NONE', ( #4670, #16506, #11297, #15901 ) ) ;
#17455=DIRECTION ( 'NONE',  ( 1.000000000000000000, 0.000000000000000000, 0.000000000000000000 ) ) ;
#17469=EDGE_CURVE ( 'NONE', #8826, #14308, #21479, .T. ) ;
#17542=DIRECTION ( 'NONE',  ( 1.000000000000000000, 0.000000000000000000, 0.000000000000000000 ) ) ;
#17543=VERTEX_POINT ( 'NONE', #22747 ) ;
#17562=DIRECTION ( 'NONE',  ( -1.000000000000000000, -0.000000000000000000, -0.000000000000000000 ) ) ;
#17573=VECTOR ( 'NONE', #3761, 1000.000000000000000 ) ;
#17621=AXIS2_PLACEMENT_3D ( 'NONE', #1666, #103, #12253 ) ;
#17633=CARTESIAN_POINT ( 'NONE',  ( -2.999999999999998668, 2.486033002269127373E-15, 20.30000000000000071 ) ) ;
#17653=EDGE_CURVE ( 'NONE', #5300, #5262, #12682, .T. ) ;
#17753=AXIS2_PLACEMENT_3D ( 'NONE', #9821, #1096, #12031 ) ;
#17757=ORIENTED_EDGE ( 'NONE', *, *, #6983, .F. ) ;
#17799=ORIENTED_EDGE ( 'NONE', *, *, #6983, .T. ) ;
#17816=DIRECTION ( 'NONE',  ( 1.000000000000000000, 0.000000000000000000, 0.000000000000000000 ) ) ;
#17846=VERTEX_POINT ( 'NONE', #10930 ) ;
#17954=CARTESIAN_POINT ( 'NONE',  ( -20.63749999999999574, 0.000000000000000000, -25.00000000000000000 ) ) ;
#17990=DIRECTION ( 'NONE',  ( 0.000000000000000000, 0.000000000000000000, -1.000000000000000000 ) ) ;
#18047=CARTESIAN_POINT ( 'NONE',  ( 0.2727178028658734932, 0.000000000000000000, 21.02499999999999503 ) ) ;
#18053=AXIS2_PLACEMENT_3D ( 'NONE', #6846, #10736, #1407 ) ;
#18069=ADVANCED_FACE ( 'NONE', ( #20539 ), #20659, .F. ) ;
#18098=AXIS2_PLACEMENT_3D ( 'NONE', #18504, #3890, #5702 ) ;
#18121=CARTESIAN_POINT ( 'NONE',  ( 2.699999999999995737, 2.486033002269127373E-15, 20.30000000000000071 ) ) ;
#18148=VERTEX_POINT ( 'NONE', #17633 ) ;
#18171=ADVANCED_FACE ( 'NONE', ( #13709, #2889 ), #21145, .T. ) ;
#18182=DIRECTION ( 'NONE',  ( 0.000000000000000000, 0.000000000000000000, -1.000000000000000000 ) ) ;
#18213=ORIENTED_EDGE ( 'NONE', *, *, #3507, .F. ) ;
#18223=CARTESIAN_POINT ( 'NONE',  ( 0.000000000000000000, 0.000000000000000000, 22.50000000000000000 ) ) ;
#18243=( NAMED_UNIT ( * ) PLANE_ANGLE_UNIT ( ) SI_UNIT ( $, .RADIAN. ) );
#18248=CARTESIAN_POINT ( 'NONE',  ( -20.63749999999999574, 0.000000000000000000, 0.000000000000000000 ) ) ;
#18384=DIRECTION ( 'NONE',  ( 0.000000000000000000, 0.000000000000000000, -1.000000000000000000 ) ) ;
#18427=VERTEX_POINT ( 'NONE', #220 ) ;
#18429=AXIS2_PLACEMENT_3D ( 'NONE', #1626, #22031, #12903 ) ;
#18464=DIRECTION ( 'NONE',  ( 0.000000000000000000, 1.000000000000000000, -1.224646799147353207E-16 ) ) ;
#18497=CARTESIAN_POINT ( 'NONE',  ( -2.999999999999995559, 0.000000000000000000, 0.000000000000000000 ) ) ;
#18504=CARTESIAN_POINT ( 'NONE',  ( 0.000000000000000000, 0.000000000000000000, 22.50000000000000000 ) ) ;
#18520=CARTESIAN_POINT ( 'NONE',  ( -20.63749999999999929, 0.000000000000000000, 0.000000000000000000 ) ) ;
#18542=DIRECTION ( 'NONE',  ( 1.000000000000000000, 0.000000000000000000, 0.000000000000000000 ) ) ;
#18592=DIRECTION ( 'NONE',  ( 0.000000000000000000, 0.000000000000000000, 1.000000000000000000 ) ) ;
#18636=ORIENTED_EDGE ( 'NONE', *, *, #13672, .T. ) ;
#18659=DIRECTION ( 'NONE',  ( 1.000000000000000000, 0.000000000000000000, 0.000000000000000000 ) ) ;
#18692=CARTESIAN_POINT ( 'NONE',  ( -2.700000000000001510, 0.000000000000000000, 0.000000000000000000 ) ) ;
#18695=ORIENTED_EDGE ( 'NONE', *, *, #6799, .F. ) ;
#18747=AXIS2_PLACEMENT_3D ( 'NONE', #11019, #5441, #1328 ) ;
#18780=CYLINDRICAL_SURFACE ( 'NONE', #16515, 25.00000000000000000 ) ;
#18813=CARTESIAN_POINT ( 'NONE',  ( 1.118033988749894458, 2.877919977996280320E-15, -23.50000000000000000 ) ) ;
#18969=ORIENTED_EDGE ( 'NONE', *, *, #13281, .T. ) ;
#18996=ORIENTED_EDGE ( 'NONE', *, *, #8611, .T. ) ;
#19026=DIRECTION ( 'NONE',  ( 0.000000000000000000, 0.000000000000000000, 1.000000000000000000 ) ) ;
#19032=CARTESIAN_POINT ( 'NONE',  ( -3.000000000000002665, 2.936090700955779358E-15, 23.97500000000000142 ) ) ;
#19121=EDGE_LOOP ( 'NONE', ( #73, #7755, #22393, #9657 ) ) ;
#19193=( NAMED_UNIT ( * ) SI_UNIT ( $, .STERADIAN. ) SOLID_ANGLE_UNIT ( ) );
#19208=ORIENTED_EDGE ( 'NONE', *, *, #23350, .F. ) ;
#19211=DIRECTION ( 'NONE',  ( 0.000000000000000000, 0.000000000000000000, -1.000000000000000000 ) ) ;
#19258=DIRECTION ( 'NONE',  ( 0.000000000000000000, 0.000000000000000000, -1.000000000000000000 ) ) ;
#19335=( NAMED_UNIT ( * ) PLANE_ANGLE_UNIT ( ) SI_UNIT ( $, .RADIAN. ) );
#19347=CARTESIAN_POINT ( 'NONE',  ( -2.999999999999995559, 0.000000000000000000, 0.000000000000000000 ) ) ;
#19368=DIRECTION ( 'NONE',  ( 0.000000000000000000, 1.000000000000000000, -1.224646799147353207E-16 ) ) ;
#19387=CARTESIAN_POINT ( 'NONE',  ( -20.63749999999999574, 0.000000000000000000, -23.50000000000000000 ) ) ;
#19413=DIRECTION ( 'NONE',  ( -1.000000000000000000, 0.000000000000000000, -0.000000000000000000 ) ) ;
#19486=ORIENTED_EDGE ( 'NONE', *, *, #22375, .T. ) ;
#19567=ORIENTED_EDGE ( 'NONE', *, *, #8047, .T. ) ;
#19658=CARTESIAN_POINT ( 'NONE',  ( 2.699999999999997513, 2.467663300281916154E-15, 19.99999999999998934 ) ) ;
#19661=DIRECTION ( 'NONE',  ( 0.000000000000000000, 0.000000000000000000, -1.000000000000000000 ) ) ;
#19728=DIRECTION ( 'NONE',  ( 0.000000000000000000, -1.224646799147351975E-16, 1.000000000000000000 ) ) ;
#19732=EDGE_CURVE ( 'NONE', #17846, #4308, #10614, .T. ) ;
#19780=AXIS2_PLACEMENT_3D ( 'NONE', #3922, #18542, #560 ) ;
#19827=DIRECTION ( 'NONE',  ( 0.000000000000000000, 1.000000000000000000, -1.224646799147353207E-16 ) ) ;
#19851=CARTESIAN_POINT ( 'NONE',  ( -2.999999999999995559, 0.000000000000000000, -21.50000000000000000 ) ) ;
#19853=DIRECTION ( 'NONE',  ( 1.000000000000000000, 0.000000000000000000, 0.000000000000000000 ) ) ;
#19885=VERTEX_POINT ( 'NONE', #2105 ) ;
#20104=CARTESIAN_POINT ( 'NONE',  ( -20.63749999999999929, 0.000000000000000000, 0.000000000000000000 ) ) ;
#20260=DIRECTION ( 'NONE',  ( 0.000000000000000000, 1.224646799147357891E-16, 1.000000000000000000 ) ) ;
#20279=MANIFOLD_SOLID_BREP ( 'OuterRace', #12214 ) ;
#20294=VERTEX_POINT ( 'NONE', #3896 ) ;
#20312=DIRECTION ( 'NONE',  ( 1.000000000000000000, 0.000000000000000000, 0.000000000000000000 ) ) ;
#20313=EDGE_CURVE ( 'NONE', #23227, #23365, #3003, .T. ) ;
#20330=CARTESIAN_POINT ( 'NONE',  ( -20.63749999999999929, 2.632990618166809235E-15, 21.50000000000000000 ) ) ;
#20410=FACE_OUTER_BOUND ( 'NONE', #15391, .T. ) ;
#20469=CARTESIAN_POINT ( 'NONE',  ( -2.999999999999995559, 0.000000000000000000, 0.000000000000000000 ) ) ;
#20539=FACE_OUTER_BOUND ( 'NONE', #5268, .T. ) ;
#20554=CARTESIAN_POINT ( 'NONE',  ( 2.700000000000001510, 0.000000000000000000, 0.000000000000000000 ) ) ;
#20597=DIRECTION ( 'NONE',  ( 1.000000000000000000, 0.000000000000000000, 0.000000000000000000 ) ) ;
#20614=CARTESIAN_POINT ( 'NONE',  ( -3.000000000000002665, 3.043247295881173007E-15, 24.69999999999999929 ) ) ;
#20647=( LENGTH_UNIT ( ) NAMED_UNIT ( * ) SI_UNIT ( .MILLI., .METRE. ) );
#20659=CYLINDRICAL_SURFACE ( 'NONE', #12304, 23.97500000000000497 ) ;
#20698=EDGE_CURVE ( 'NONE', #14308, #17543, #1474, .T. ) ;
#20719=ORIENTED_EDGE ( 'NONE', *, *, #7716, .F. ) ;
#20731=VERTEX_POINT ( 'NONE', #4920 ) ;
#20733=AXIS2_PLACEMENT_3D ( 'NONE', #3279, #10689, #16337 ) ;
#20739=DIRECTION ( 'NONE',  ( 0.000000000000000000, 0.000000000000000000, -1.000000000000000000 ) ) ;
#20830=AXIS2_PLACEMENT_3D ( 'NONE', #18520, #20312, #3904 ) ;
#21022=VECTOR ( 'NONE', #21613, 1000.000000000000000 ) ;
#21029=AXIS2_PLACEMENT_3D ( 'NONE', #21382, #744, #6297 ) ;
#21039=CARTESIAN_POINT ( 'NONE',  ( -0.2727178028658734932, 0.000000000000000000, 0.000000000000000000 ) ) ;
#21051=CIRCLE ( 'NONE', #11049, 0.3000000000000051514 ) ;
#21081=VERTEX_POINT ( 'NONE', #671 ) ;
#21082=ORIENTED_EDGE ( 'NONE', *, *, #13505, .F. ) ;
#21086=ORIENTED_EDGE ( 'NONE', *, *, #8611, .F. ) ;
#21136=CIRCLE ( 'NONE', #13851, 23.97500000000000142 ) ;
#21141=ADVANCED_FACE ( 'NONE', ( #13527 ), #8763, .T. ) ;
#21145=PLANE ( 'NONE',  #21029 ) ;
#21160=DIRECTION ( 'NONE',  ( 0.000000000000000000, 0.000000000000000000, -1.000000000000000000 ) ) ;
#21249=EDGE_CURVE ( 'NONE', #21081, #15926, #21568, .T. ) ;
#21270=ORIENTED_EDGE ( 'NONE', *, *, #1975, .F. ) ;
#21286=VERTEX_POINT ( 'NONE', #10947 ) ;
#21311=DIRECTION ( 'NONE',  ( 0.000000000000000000, 0.000000000000000000, 1.000000000000000000 ) ) ;
#21324=ORIENTED_EDGE ( 'NONE', *, *, #19732, .T. ) ;
#21382=CARTESIAN_POINT ( 'NONE',  ( 2.999999999999999112, 20.30000000000000071, 0.000000000000000000 ) ) ;
#21472=DIRECTION ( 'NONE',  ( 1.000000000000000000, 0.000000000000000000, 0.000000000000000000 ) ) ;
#21479=CIRCLE ( 'NONE', #7214, 19.99999999999999645 ) ;
#21481=FACE_BOUND ( 'NONE', #11981, .T. ) ;
#21495=EDGE_LOOP ( 'NONE', ( #137, #11157, #8810, #12868 ) ) ;
#21518=DIRECTION ( 'NONE',  ( 1.000000000000000000, 0.000000000000000000, 0.000000000000000000 ) ) ;
#21521=DIRECTION ( 'NONE',  ( 0.000000000000000000, 0.000000000000000000, -1.000000000000000000 ) ) ;
#21530=ADVANCED_FACE ( 'NONE', ( #13838 ), #14629, .T. ) ;
#21544=ADVANCED_FACE ( 'NONE', ( #4625 ), #16190, .T. ) ;
#21568=CIRCLE ( 'NONE', #8086, 0.3000000000000016542 ) ;
#21570=TOROIDAL_SURFACE ( 'NONE', #1515, 22.50000000000000000, 1.500000000000000444 ) ;
#21574=AXIS2_PLACEMENT_3D ( 'NONE', #7152, #1710, #3526 ) ;
#21600=AXIS2_PLACEMENT_3D ( 'NONE', #18248, #21518, #8861 ) ;
#21613=DIRECTION ( 'NONE',  ( 1.000000000000000000, 0.000000000000000000, 0.000000000000000000 ) ) ;
#21696=DIRECTION ( 'NONE',  ( -1.000000000000000000, -0.000000000000000000, -0.000000000000000000 ) ) ;
#21745=ADVANCED_FACE ( 'NONE', ( #22578 ), #23422, .T. ) ;
#21856=AXIS2_PLACEMENT_3D ( 'NONE', #22348, #12540, #13224 ) ;
#21868=DIRECTION ( 'NONE',  ( 0.000000000000000000, 1.224646799147346305E-16, 1.000000000000000000 ) ) ;
#21872=CARTESIAN_POINT ( 'NONE',  ( -20.63749999999999929, 0.000000000000000000, 0.000000000000000000 ) ) ;
#21979=CIRCLE ( 'NONE', #763, 23.50000000000000000 ) ;
#22031=DIRECTION ( 'NONE',  ( 1.000000000000000000, 0.000000000000000000, 0.000000000000000000 ) ) ;
#22052=ORIENTED_EDGE ( 'NONE', *, *, #15548, .T. ) ;
#22100=VERTEX_POINT ( 'NONE', #14009 ) ;
#22105=AXIS2_PLACEMENT_3D ( 'NONE', #13928, #19413, #22812 ) ;
#22125=DIRECTION ( 'NONE',  ( 1.000000000000000000, 0.000000000000000000, 0.000000000000000000 ) ) ;
#22138=AXIS2_PLACEMENT_3D ( 'NONE', #15177, #5977, #13386 ) ;
#22208=DIRECTION ( 'NONE',  ( 1.000000000000000000, 0.000000000000000000, 0.000000000000000000 ) ) ;
#22248=AXIS2_PLACEMENT_3D ( 'NONE', #12691, #3336, #3806 ) ;
#22293=EDGE_CURVE ( 'NONE', #22490, #23365, #6102, .T. ) ;
#22339=EDGE_CURVE ( 'NONE', #19885, #2929, #21136, .T. ) ;
#22348=CARTESIAN_POINT ( 'NONE',  ( -20.63749999999999574, 0.000000000000000000, 0.000000000000000000 ) ) ;
#22350=VERTEX_POINT ( 'NONE', #18047 ) ;
#22358=ORIENTED_EDGE ( 'NONE', *, *, #15516, .F. ) ;
#22375=EDGE_CURVE ( 'NONE', #20294, #11363, #16894, .T. ) ;
#22393=ORIENTED_EDGE ( 'NONE', *, *, #2730, .F. ) ;
#22473=DIRECTION ( 'NONE',  ( 1.000000000000000000, 0.000000000000000000, 0.000000000000000000 ) ) ;
#22490=VERTEX_POINT ( 'NONE', #19851 ) ;
#22542=CARTESIAN_POINT ( 'NONE',  ( -20.63749999999999929, 0.000000000000000000, -19.99999999999999289 ) ) ;
#22550=CARTESIAN_POINT ( 'NONE',  ( 3.000000000000002665, 0.000000000000000000, -23.50000000000000000 ) ) ;
#22578=FACE_OUTER_BOUND ( 'NONE', #10730, .T. ) ;
#22602=CARTESIAN_POINT ( 'NONE',  ( 1.118033988749894458, 0.000000000000000000, 23.50000000000000000 ) ) ;
#22693=AXIS2_PLACEMENT_3D ( 'NONE', #2937, #8282, #16008 ) ;
#22695=AXIS2_PLACEMENT_3D ( 'NONE', #7323, #3801, #5752 ) ;
#22703=AXIS2_PLACEMENT_3D ( 'NONE', #6607, #14113, #1517 ) ;
#22740=CARTESIAN_POINT ( 'NONE',  ( 2.700000000000001510, 0.000000000000000000, 0.000000000000000000 ) ) ;
#22747=CARTESIAN_POINT ( 'NONE',  ( -2.999999999999998668, 0.000000000000000000, -20.30000000000000071 ) ) ;
#22812=DIRECTION ( 'NONE',  ( -0.000000000000000000, 0.000000000000000000, 1.000000000000000000 ) ) ;
#22825=CIRCLE ( 'NONE', #9752, 25.00000000000000000 ) ;
#22852=AXIS2_PLACEMENT_3D ( 'NONE', #16855, #15306, #318 ) ;
#22853=DIRECTION ( 'NONE',  ( 0.000000000000000000, 0.000000000000000000, -1.000000000000000000 ) ) ;
#22859=EDGE_CURVE ( 'NONE', #22100, #17297, #23071, .T. ) ;
#22891=CARTESIAN_POINT ( 'NONE',  ( -2.699999999999997513, 0.000000000000000000, -19.99999999999999645 ) ) ;
#22955=DIRECTION ( 'NONE',  ( 0.000000000000000000, 0.000000000000000000, -1.000000000000000000 ) ) ;
#22969=ADVANCED_FACE ( 'NONE', ( #17023 ), #4958, .T. ) ;
#22979=CIRCLE ( 'NONE', #1761, 20.30000000000000071 ) ;
#23042=FACE_OUTER_BOUND ( 'NONE', #15691, .T. ) ;
#23071=CIRCLE ( 'NONE', #16148, 1.500000000000001332 ) ;
#23092=CIRCLE ( 'NONE', #18098, 1.500000000000001332 ) ;
#23137=DIRECTION ( 'NONE',  ( 0.000000000000000000, 0.000000000000000000, -1.000000000000000000 ) ) ;
#23204=DIRECTION ( 'NONE',  ( 1.000000000000000000, 0.000000000000000000, 0.000000000000000000 ) ) ;
#23227=VERTEX_POINT ( 'NONE', #15574 ) ;
#23265=CARTESIAN_POINT ( 'NONE',  ( -2.699999999999997513, 2.449293598294706119E-15, 19.99999999999999645 ) ) ;
#23269=PRODUCT ( 'angular contact ball bearing_68_iso_ISO 15 ABB - 1740 - 38,SI,NC,38_68', 'angular contact ball bearing_68_iso_ISO 15 ABB - 1740 - 38,SI,NC,38_68', '', ( #14736 ) ) ;
#23273=DIRECTION ( 'NONE',  ( -1.000000000000000000, 0.000000000000000000, -0.000000000000000000 ) ) ;
#23274=AXIS2_PLACEMENT_3D ( 'NONE', #14174, #10301, #15865 ) ;
#23322=EDGE_LOOP ( 'NONE', ( #13744, #18969 ) ) ;
#23350=EDGE_CURVE ( 'NONE', #5262, #5300, #6125, .T. ) ;
#23353=CARTESIAN_POINT ( 'NONE',  ( 0.000000000000000000, 2.755455298081544778E-15, -22.50000000000000000 ) ) ;
#23365=VERTEX_POINT ( 'NONE', #13167 ) ;
#23419=AXIS2_PLACEMENT_3D ( 'NONE', #2265, #11857, #20739 ) ;
#23422=TOROIDAL_SURFACE ( 'NONE', #11515, 22.50000000000000000, 1.500000000000000444 ) ;
#23440=ORIENTED_EDGE ( 'NONE', *, *, #3992, .F. ) ;
#23444=EDGE_CURVE ( 'NONE', #4308, #5940, #723, .T. ) ;
#23488=ORIENTED_EDGE ( 'NONE', *, *, #1246, .F. ) ;
#23499=AXIS2_PLACEMENT_3D ( 'NONE', #20469, #4162, #9742 ) ;
#23513=CARTESIAN_POINT ( 'NONE',  ( 0.000000000000000000, 0.000000000000000000, 0.000000000000000000 ) ) ;
#23526=EDGE_LOOP ( 'NONE', ( #3996, #727, #16699, #10349 ) ) ;
#23581=ORIENTED_EDGE ( 'NONE', *, *, #16566, .F. ) ;
#23614=ORIENTED_EDGE ( 'NONE', *, *, #8900, .T. ) ;
#23678=SURFACE_STYLE_FILL_AREA ( #12752 ) ;
#23681=AXIS2_PLACEMENT_3D ( 'NONE', #14097, #19853, #5020 ) ;
#23710=DIRECTION ( 'NONE',  ( 0.000000000000000000, 0.000000000000000000, -1.000000000000000000 ) ) ;
#23914=COLOUR_RGB('Grey',0.48,0.52,0.57);
#23915=FILL_AREA_STYLE_COLOUR('',#23914);
#23916=FILL_AREA_STYLE('',(#23915));
#23917=SURFACE_STYLE_FILL_AREA(#23916);
#23918=SURFACE_SIDE_STYLE('',(#23917));
#23919=SURFACE_STYLE_USAGE(.BOTH.,#23918);
#23920=PRESENTATION_STYLE_ASSIGNMENT((#23919));
ENDSEC;
END-ISO-10303-21;
